ISO-10303-21;
HEADER;
/* Generated by software containing ST-Developer
 * from STEP Tools, Inc. (www.steptools.com) 
 */

FILE_DESCRIPTION(
/* description */ ('Located fixture plate with toggle clamp'),
/* implementation_level */ '2;1');

FILE_NAME(
/* name */ 'M5x14 Cap Screw (1).step',
/* time_stamp */ '2026-10-27T21:36:12-07:00',
/* author */ (''),
/* organization */ (''),
/* preprocessor_version */ 'ST-DEVELOPER v20.2',
/* originating_system */ 'Autodesk Translation Framework v15.17.0.0',
/* authorisation */ '');

FILE_SCHEMA (('AUTOMOTIVE_DESIGN { 1 0 10303 214 3 1 1 }'));
ENDSEC;

DATA;
#10=MECHANICAL_DESIGN_GEOMETRIC_PRESENTATION_REPRESENTATION('',(#335),#9285);
#246=ORIENTED_CLOSED_SHELL('',*,#5185,.F.);
#249=BREP_WITH_VOIDS('Body1',#5186,(#246));
#264=CONICAL_SURFACE('',#5845,0.4,0.785398163397448);
#265=CONICAL_SURFACE('',#5849,0.41,0.785398163397448);
#266=CONICAL_SURFACE('',#5853,0.26,0.463647609000806);
#287=SHAPE_REPRESENTATION_RELATIONSHIP('SRR','None',#9411,#311);
#311=ADVANCED_BREP_SHAPE_REPRESENTATION('',(#249),#9273);
#335=STYLED_ITEM('',(#9619),#249);
#465=FACE_BOUND('',#1289,.T.);
#617=PLANE('',#5833);
#618=PLANE('',#5834);
#619=PLANE('',#5835);
#620=PLANE('',#5836);
#621=PLANE('',#5837);
#622=PLANE('',#5838);
#623=PLANE('',#5839);
#624=PLANE('',#5840);
#625=PLANE('',#5841);
#626=PLANE('',#5843);
#627=PLANE('',#5851);
#881=FACE_OUTER_BOUND('',#1275,.T.);
#882=FACE_OUTER_BOUND('',#1276,.T.);
#883=FACE_OUTER_BOUND('',#1277,.T.);
#884=FACE_OUTER_BOUND('',#1278,.T.);
#885=FACE_OUTER_BOUND('',#1279,.T.);
#886=FACE_OUTER_BOUND('',#1280,.T.);
#887=FACE_OUTER_BOUND('',#1281,.T.);
#888=FACE_OUTER_BOUND('',#1282,.T.);
#889=FACE_OUTER_BOUND('',#1283,.T.);
#890=FACE_OUTER_BOUND('',#1284,.T.);
#891=FACE_OUTER_BOUND('',#1285,.T.);
#892=FACE_OUTER_BOUND('',#1286,.T.);
#893=FACE_OUTER_BOUND('',#1287,.T.);
#894=FACE_OUTER_BOUND('',#1288,.T.);
#895=FACE_OUTER_BOUND('',#1290,.T.);
#896=FACE_OUTER_BOUND('',#1291,.T.);
#1275=EDGE_LOOP('',(#4438,#4439,#4440,#4441));
#1276=EDGE_LOOP('',(#4442,#4443,#4444,#4445));
#1277=EDGE_LOOP('',(#4446,#4447,#4448,#4449));
#1278=EDGE_LOOP('',(#4450,#4451,#4452,#4453));
#1279=EDGE_LOOP('',(#4454,#4455,#4456,#4457));
#1280=EDGE_LOOP('',(#4458,#4459,#4460,#4461));
#1281=EDGE_LOOP('',(#4462,#4463,#4464,#4465,#4466,#4467));
#1282=EDGE_LOOP('',(#4468,#4469,#4470,#4471,#4472,#4473));
#1283=EDGE_LOOP('',(#4474));
#1284=EDGE_LOOP('',(#4475));
#1285=EDGE_LOOP('',(#4476,#4477,#4478,#4479));
#1286=EDGE_LOOP('',(#4480,#4481,#4482,#4483));
#1287=EDGE_LOOP('',(#4484,#4485,#4486,#4487));
#1288=EDGE_LOOP('',(#4488));
#1289=EDGE_LOOP('',(#4489));
#1290=EDGE_LOOP('',(#4490,#4491,#4492,#4493));
#1291=EDGE_LOOP('',(#4494,#4495,#4496,#4497));
#1529=CIRCLE('',#5842,0.24505);
#1530=CIRCLE('',#5844,0.375);
#1531=CIRCLE('',#5846,0.425);
#1532=CIRCLE('',#5848,0.425);
#1533=CIRCLE('',#5850,0.395);
#1534=CIRCLE('',#5852,0.27);
#1535=CIRCLE('',#5854,0.24505);
#1890=LINE('',#8639,#2300);
#1891=LINE('',#8641,#2301);
#1892=LINE('',#8643,#2302);
#1893=LINE('',#8644,#2303);
#1894=LINE('',#8647,#2304);
#1895=LINE('',#8649,#2305);
#1896=LINE('',#8650,#2306);
#1897=LINE('',#8653,#2307);
#1898=LINE('',#8655,#2308);
#1899=LINE('',#8656,#2309);
#1900=LINE('',#8659,#2310);
#1901=LINE('',#8661,#2311);
#1902=LINE('',#8662,#2312);
#1903=LINE('',#8665,#2313);
#1904=LINE('',#8667,#2314);
#1905=LINE('',#8668,#2315);
#1906=LINE('',#8670,#2316);
#1907=LINE('',#8671,#2317);
#1908=LINE('',#8683,#2318);
#1909=LINE('',#8687,#2319);
#1910=LINE('',#8691,#2320);
#1911=LINE('',#8698,#2321);
#1912=LINE('',#8700,#2322);
#2300=VECTOR('',#7084,1.);
#2301=VECTOR('',#7085,1.);
#2302=VECTOR('',#7086,1.);
#2303=VECTOR('',#7087,1.);
#2304=VECTOR('',#7090,1.);
#2305=VECTOR('',#7091,1.);
#2306=VECTOR('',#7092,1.);
#2307=VECTOR('',#7095,1.);
#2308=VECTOR('',#7096,1.);
#2309=VECTOR('',#7097,1.);
#2310=VECTOR('',#7100,1.);
#2311=VECTOR('',#7101,1.);
#2312=VECTOR('',#7102,1.);
#2313=VECTOR('',#7105,1.);
#2314=VECTOR('',#7106,1.);
#2315=VECTOR('',#7107,1.);
#2316=VECTOR('',#7110,1.);
#2317=VECTOR('',#7111,1.);
#2318=VECTOR('',#7128,0.4);
#2319=VECTOR('',#7133,0.425);
#2320=VECTOR('',#7138,0.41);
#2321=VECTOR('',#7147,0.26);
#2322=VECTOR('',#7150,0.25);
#2715=VERTEX_POINT('',#8637);
#2716=VERTEX_POINT('',#8638);
#2717=VERTEX_POINT('',#8640);
#2718=VERTEX_POINT('',#8642);
#2719=VERTEX_POINT('',#8646);
#2720=VERTEX_POINT('',#8648);
#2721=VERTEX_POINT('',#8652);
#2722=VERTEX_POINT('',#8654);
#2723=VERTEX_POINT('',#8658);
#2724=VERTEX_POINT('',#8660);
#2725=VERTEX_POINT('',#8664);
#2726=VERTEX_POINT('',#8666);
#2727=VERTEX_POINT('',#8675);
#2728=VERTEX_POINT('',#8678);
#2729=VERTEX_POINT('',#8681);
#2730=VERTEX_POINT('',#8685);
#2731=VERTEX_POINT('',#8689);
#2732=VERTEX_POINT('',#8693);
#2733=VERTEX_POINT('',#8696);
#3307=EDGE_CURVE('',#2715,#2716,#1890,.T.);
#3308=EDGE_CURVE('',#2716,#2717,#1891,.T.);
#3309=EDGE_CURVE('',#2717,#2718,#1892,.T.);
#3310=EDGE_CURVE('',#2715,#2718,#1893,.T.);
#3311=EDGE_CURVE('',#2716,#2719,#1894,.T.);
#3312=EDGE_CURVE('',#2719,#2720,#1895,.T.);
#3313=EDGE_CURVE('',#2720,#2717,#1896,.T.);
#3314=EDGE_CURVE('',#2719,#2721,#1897,.T.);
#3315=EDGE_CURVE('',#2721,#2722,#1898,.T.);
#3316=EDGE_CURVE('',#2722,#2720,#1899,.T.);
#3317=EDGE_CURVE('',#2721,#2723,#1900,.T.);
#3318=EDGE_CURVE('',#2723,#2724,#1901,.T.);
#3319=EDGE_CURVE('',#2724,#2722,#1902,.T.);
#3320=EDGE_CURVE('',#2723,#2725,#1903,.T.);
#3321=EDGE_CURVE('',#2725,#2726,#1904,.T.);
#3322=EDGE_CURVE('',#2726,#2724,#1905,.T.);
#3323=EDGE_CURVE('',#2725,#2715,#1906,.T.);
#3324=EDGE_CURVE('',#2718,#2726,#1907,.T.);
#3325=EDGE_CURVE('',#2727,#2727,#1529,.T.);
#3326=EDGE_CURVE('',#2728,#2728,#1530,.T.);
#3327=EDGE_CURVE('',#2729,#2729,#1531,.T.);
#3328=EDGE_CURVE('',#2729,#2728,#1908,.T.);
#3329=EDGE_CURVE('',#2730,#2730,#1532,.T.);
#3330=EDGE_CURVE('',#2730,#2729,#1909,.T.);
#3331=EDGE_CURVE('',#2731,#2731,#1533,.T.);
#3332=EDGE_CURVE('',#2731,#2730,#1910,.T.);
#3333=EDGE_CURVE('',#2732,#2732,#1534,.T.);
#3334=EDGE_CURVE('',#2733,#2733,#1535,.F.);
#3335=EDGE_CURVE('',#2733,#2732,#1911,.T.);
#3336=EDGE_CURVE('',#2727,#2733,#1912,.T.);
#4438=ORIENTED_EDGE('',*,*,#3307,.T.);
#4439=ORIENTED_EDGE('',*,*,#3308,.T.);
#4440=ORIENTED_EDGE('',*,*,#3309,.T.);
#4441=ORIENTED_EDGE('',*,*,#3310,.F.);
#4442=ORIENTED_EDGE('',*,*,#3311,.T.);
#4443=ORIENTED_EDGE('',*,*,#3312,.T.);
#4444=ORIENTED_EDGE('',*,*,#3313,.T.);
#4445=ORIENTED_EDGE('',*,*,#3308,.F.);
#4446=ORIENTED_EDGE('',*,*,#3314,.T.);
#4447=ORIENTED_EDGE('',*,*,#3315,.T.);
#4448=ORIENTED_EDGE('',*,*,#3316,.T.);
#4449=ORIENTED_EDGE('',*,*,#3312,.F.);
#4450=ORIENTED_EDGE('',*,*,#3317,.T.);
#4451=ORIENTED_EDGE('',*,*,#3318,.T.);
#4452=ORIENTED_EDGE('',*,*,#3319,.T.);
#4453=ORIENTED_EDGE('',*,*,#3315,.F.);
#4454=ORIENTED_EDGE('',*,*,#3320,.T.);
#4455=ORIENTED_EDGE('',*,*,#3321,.T.);
#4456=ORIENTED_EDGE('',*,*,#3322,.T.);
#4457=ORIENTED_EDGE('',*,*,#3318,.F.);
#4458=ORIENTED_EDGE('',*,*,#3323,.T.);
#4459=ORIENTED_EDGE('',*,*,#3310,.T.);
#4460=ORIENTED_EDGE('',*,*,#3324,.T.);
#4461=ORIENTED_EDGE('',*,*,#3321,.F.);
#4462=ORIENTED_EDGE('',*,*,#3323,.F.);
#4463=ORIENTED_EDGE('',*,*,#3320,.F.);
#4464=ORIENTED_EDGE('',*,*,#3317,.F.);
#4465=ORIENTED_EDGE('',*,*,#3314,.F.);
#4466=ORIENTED_EDGE('',*,*,#3311,.F.);
#4467=ORIENTED_EDGE('',*,*,#3307,.F.);
#4468=ORIENTED_EDGE('',*,*,#3324,.F.);
#4469=ORIENTED_EDGE('',*,*,#3309,.F.);
#4470=ORIENTED_EDGE('',*,*,#3313,.F.);
#4471=ORIENTED_EDGE('',*,*,#3316,.F.);
#4472=ORIENTED_EDGE('',*,*,#3319,.F.);
#4473=ORIENTED_EDGE('',*,*,#3322,.F.);
#4474=ORIENTED_EDGE('',*,*,#3325,.F.);
#4475=ORIENTED_EDGE('',*,*,#3326,.F.);
#4476=ORIENTED_EDGE('',*,*,#3327,.F.);
#4477=ORIENTED_EDGE('',*,*,#3328,.T.);
#4478=ORIENTED_EDGE('',*,*,#3326,.T.);
#4479=ORIENTED_EDGE('',*,*,#3328,.F.);
#4480=ORIENTED_EDGE('',*,*,#3329,.F.);
#4481=ORIENTED_EDGE('',*,*,#3330,.T.);
#4482=ORIENTED_EDGE('',*,*,#3327,.T.);
#4483=ORIENTED_EDGE('',*,*,#3330,.F.);
#4484=ORIENTED_EDGE('',*,*,#3331,.F.);
#4485=ORIENTED_EDGE('',*,*,#3332,.T.);
#4486=ORIENTED_EDGE('',*,*,#3329,.T.);
#4487=ORIENTED_EDGE('',*,*,#3332,.F.);
#4488=ORIENTED_EDGE('',*,*,#3331,.T.);
#4489=ORIENTED_EDGE('',*,*,#3333,.F.);
#4490=ORIENTED_EDGE('',*,*,#3334,.F.);
#4491=ORIENTED_EDGE('',*,*,#3335,.T.);
#4492=ORIENTED_EDGE('',*,*,#3333,.T.);
#4493=ORIENTED_EDGE('',*,*,#3335,.F.);
#4494=ORIENTED_EDGE('',*,*,#3325,.T.);
#4495=ORIENTED_EDGE('',*,*,#3336,.T.);
#4496=ORIENTED_EDGE('',*,*,#3334,.T.);
#4497=ORIENTED_EDGE('',*,*,#3336,.F.);
#4853=CYLINDRICAL_SURFACE('',#5847,0.425);
#4854=CYLINDRICAL_SURFACE('',#5855,0.24505);
#5082=ADVANCED_FACE('',(#881),#617,.F.);
#5083=ADVANCED_FACE('',(#882),#618,.F.);
#5084=ADVANCED_FACE('',(#883),#619,.F.);
#5085=ADVANCED_FACE('',(#884),#620,.F.);
#5086=ADVANCED_FACE('',(#885),#621,.F.);
#5087=ADVANCED_FACE('',(#886),#622,.F.);
#5088=ADVANCED_FACE('',(#887),#623,.F.);
#5089=ADVANCED_FACE('',(#888),#624,.F.);
#5090=ADVANCED_FACE('',(#889),#625,.F.);
#5091=ADVANCED_FACE('',(#890),#626,.T.);
#5092=ADVANCED_FACE('',(#891),#264,.T.);
#5093=ADVANCED_FACE('',(#892),#4853,.T.);
#5094=ADVANCED_FACE('',(#893),#265,.T.);
#5095=ADVANCED_FACE('',(#894,#465),#627,.T.);
#5096=ADVANCED_FACE('',(#895),#266,.T.);
#5097=ADVANCED_FACE('',(#896),#4854,.T.);
#5185=CLOSED_SHELL('',(#5082,#5083,#5084,#5085,#5086,#5087,#5088,#5089));
#5186=CLOSED_SHELL('',(#5090,#5091,#5092,#5093,#5094,#5095,#5096,#5097));
#5832=AXIS2_PLACEMENT_3D('',#8635,#7080,#7081);
#5833=AXIS2_PLACEMENT_3D('',#8636,#7082,#7083);
#5834=AXIS2_PLACEMENT_3D('',#8645,#7088,#7089);
#5835=AXIS2_PLACEMENT_3D('',#8651,#7093,#7094);
#5836=AXIS2_PLACEMENT_3D('',#8657,#7098,#7099);
#5837=AXIS2_PLACEMENT_3D('',#8663,#7103,#7104);
#5838=AXIS2_PLACEMENT_3D('',#8669,#7108,#7109);
#5839=AXIS2_PLACEMENT_3D('',#8672,#7112,#7113);
#5840=AXIS2_PLACEMENT_3D('',#8673,#7114,#7115);
#5841=AXIS2_PLACEMENT_3D('',#8674,#7116,#7117);
#5842=AXIS2_PLACEMENT_3D('',#8676,#7118,#7119);
#5843=AXIS2_PLACEMENT_3D('',#8677,#7120,#7121);
#5844=AXIS2_PLACEMENT_3D('',#8679,#7122,#7123);
#5845=AXIS2_PLACEMENT_3D('',#8680,#7124,#7125);
#5846=AXIS2_PLACEMENT_3D('',#8682,#7126,#7127);
#5847=AXIS2_PLACEMENT_3D('',#8684,#7129,#7130);
#5848=AXIS2_PLACEMENT_3D('',#8686,#7131,#7132);
#5849=AXIS2_PLACEMENT_3D('',#8688,#7134,#7135);
#5850=AXIS2_PLACEMENT_3D('',#8690,#7136,#7137);
#5851=AXIS2_PLACEMENT_3D('',#8692,#7139,#7140);
#5852=AXIS2_PLACEMENT_3D('',#8694,#7141,#7142);
#5853=AXIS2_PLACEMENT_3D('',#8695,#7143,#7144);
#5854=AXIS2_PLACEMENT_3D('',#8697,#7145,#7146);
#5855=AXIS2_PLACEMENT_3D('',#8699,#7148,#7149);
#7080=DIRECTION('axis',(0.,0.,1.));
#7081=DIRECTION('refdir',(1.,0.,0.));
#7082=DIRECTION('center_axis',(0.866025403784439,0.,-0.5));
#7083=DIRECTION('ref_axis',(0.5,0.,0.866025403784439));
#7084=DIRECTION('',(-0.5,0.,-0.866025403784439));
#7085=DIRECTION('',(0.,-1.,0.));
#7086=DIRECTION('',(0.5,0.,0.866025403784439));
#7087=DIRECTION('',(0.,-1.,0.));
#7088=DIRECTION('center_axis',(1.20185167898973E-16,0.,-1.));
#7089=DIRECTION('ref_axis',(1.,0.,1.20185167898973E-16));
#7090=DIRECTION('',(-1.,0.,-1.20185167898973E-16));
#7091=DIRECTION('',(0.,-1.,0.));
#7092=DIRECTION('',(1.,0.,1.20185167898973E-16));
#7093=DIRECTION('center_axis',(-0.866025403784439,0.,-0.5));
#7094=DIRECTION('ref_axis',(0.5,0.,-0.866025403784439));
#7095=DIRECTION('',(-0.5,0.,0.866025403784439));
#7096=DIRECTION('',(0.,-1.,0.));
#7097=DIRECTION('',(0.5,0.,-0.866025403784439));
#7098=DIRECTION('center_axis',(-0.866025403784439,0.,0.5));
#7099=DIRECTION('ref_axis',(-0.5,0.,-0.866025403784439));
#7100=DIRECTION('',(0.5,0.,0.866025403784439));
#7101=DIRECTION('',(0.,-1.,0.));
#7102=DIRECTION('',(-0.5,0.,-0.866025403784439));
#7103=DIRECTION('center_axis',(-2.40370335797945E-16,0.,1.));
#7104=DIRECTION('ref_axis',(-1.,0.,-2.40370335797945E-16));
#7105=DIRECTION('',(1.,0.,2.40370335797945E-16));
#7106=DIRECTION('',(0.,-1.,0.));
#7107=DIRECTION('',(-1.,0.,-2.40370335797945E-16));
#7108=DIRECTION('center_axis',(0.866025403784439,0.,0.5));
#7109=DIRECTION('ref_axis',(-0.5,0.,0.866025403784439));
#7110=DIRECTION('',(0.5,0.,-0.866025403784439));
#7111=DIRECTION('',(-0.5,0.,0.866025403784439));
#7112=DIRECTION('center_axis',(0.,1.,0.));
#7113=DIRECTION('ref_axis',(1.,0.,0.));
#7114=DIRECTION('center_axis',(0.,-1.,0.));
#7115=DIRECTION('ref_axis',(0.,0.,-1.));
#7116=DIRECTION('center_axis',(0.,1.,0.));
#7117=DIRECTION('ref_axis',(1.,0.,0.));
#7118=DIRECTION('center_axis',(0.,1.,0.));
#7119=DIRECTION('ref_axis',(1.,0.,0.));
#7120=DIRECTION('center_axis',(0.,1.,0.));
#7121=DIRECTION('ref_axis',(0.,0.,1.));
#7122=DIRECTION('center_axis',(0.,-1.,0.));
#7123=DIRECTION('ref_axis',(1.,0.,0.));
#7124=DIRECTION('center_axis',(0.,-1.,0.));
#7125=DIRECTION('ref_axis',(1.,0.,0.));
#7126=DIRECTION('center_axis',(0.,-1.,0.));
#7127=DIRECTION('ref_axis',(1.,0.,0.));
#7128=DIRECTION('',(0.707106781186548,0.707106781186547,8.65956056235493E-17));
#7129=DIRECTION('center_axis',(0.,-1.,0.));
#7130=DIRECTION('ref_axis',(1.,0.,0.));
#7131=DIRECTION('center_axis',(0.,-1.,0.));
#7132=DIRECTION('ref_axis',(1.,0.,0.));
#7133=DIRECTION('',(0.,1.,0.));
#7134=DIRECTION('center_axis',(0.,1.,0.));
#7135=DIRECTION('ref_axis',(1.,0.,0.));
#7136=DIRECTION('center_axis',(0.,-1.,0.));
#7137=DIRECTION('ref_axis',(1.,0.,0.));
#7138=DIRECTION('',(-0.707106781186547,0.707106781186548,-8.65956056235493E-17));
#7139=DIRECTION('center_axis',(0.,-1.,0.));
#7140=DIRECTION('ref_axis',(0.,0.,-1.));
#7141=DIRECTION('center_axis',(0.,-1.,0.));
#7142=DIRECTION('ref_axis',(1.,0.,0.));
#7143=DIRECTION('center_axis',(0.,1.,0.));
#7144=DIRECTION('ref_axis',(1.,0.,0.));
#7145=DIRECTION('center_axis',(0.,1.,0.));
#7146=DIRECTION('ref_axis',(1.,0.,0.));
#7147=DIRECTION('',(-0.447213595499958,0.894427190999916,-5.47678698264203E-17));
#7148=DIRECTION('center_axis',(0.,-1.,0.));
#7149=DIRECTION('ref_axis',(1.,0.,0.));
#7150=DIRECTION('',(0.,1.,0.));
#8635=CARTESIAN_POINT('',(0.,0.,0.));
#8636=CARTESIAN_POINT('Origin',(0.115470053837925,-0.5,-0.2));
#8637=CARTESIAN_POINT('',(0.23094010767585,-0.5,0.));
#8638=CARTESIAN_POINT('',(0.115470053837925,-0.5,-0.2));
#8639=CARTESIAN_POINT('',(0.23094010767585,-0.5,0.));
#8640=CARTESIAN_POINT('',(0.115470053837925,-0.8,-0.2));
#8641=CARTESIAN_POINT('',(0.115470053837925,-0.5,-0.2));
#8642=CARTESIAN_POINT('',(0.23094010767585,-0.8,0.));
#8643=CARTESIAN_POINT('',(0.23094010767585,-0.8,0.));
#8644=CARTESIAN_POINT('',(0.23094010767585,-0.5,0.));
#8645=CARTESIAN_POINT('Origin',(-0.115470053837925,-0.5,-0.2));
#8646=CARTESIAN_POINT('',(-0.115470053837925,-0.5,-0.2));
#8647=CARTESIAN_POINT('',(0.115470053837925,-0.5,-0.2));
#8648=CARTESIAN_POINT('',(-0.115470053837925,-0.8,-0.2));
#8649=CARTESIAN_POINT('',(-0.115470053837925,-0.5,-0.2));
#8650=CARTESIAN_POINT('',(0.115470053837925,-0.8,-0.2));
#8651=CARTESIAN_POINT('Origin',(-0.23094010767585,-0.5,-2.77555756156289E-17));
#8652=CARTESIAN_POINT('',(-0.23094010767585,-0.5,-2.82820063659975E-17));
#8653=CARTESIAN_POINT('',(-0.115470053837925,-0.5,-0.2));
#8654=CARTESIAN_POINT('',(-0.23094010767585,-0.8,-2.77555756156289E-17));
#8655=CARTESIAN_POINT('',(-0.23094010767585,-0.5,-2.82820063659975E-17));
#8656=CARTESIAN_POINT('',(-0.115470053837925,-0.8,-0.2));
#8657=CARTESIAN_POINT('Origin',(-0.115470053837925,-0.5,0.2));
#8658=CARTESIAN_POINT('',(-0.115470053837925,-0.5,0.2));
#8659=CARTESIAN_POINT('',(-0.23094010767585,-0.5,-2.82820063659975E-17));
#8660=CARTESIAN_POINT('',(-0.115470053837925,-0.8,0.2));
#8661=CARTESIAN_POINT('',(-0.115470053837925,-0.5,0.2));
#8662=CARTESIAN_POINT('',(-0.23094010767585,-0.8,-2.82820063659975E-17));
#8663=CARTESIAN_POINT('Origin',(0.115470053837925,-0.5,0.2));
#8664=CARTESIAN_POINT('',(0.115470053837925,-0.5,0.2));
#8665=CARTESIAN_POINT('',(-0.115470053837925,-0.5,0.2));
#8666=CARTESIAN_POINT('',(0.115470053837925,-0.8,0.2));
#8667=CARTESIAN_POINT('',(0.115470053837925,-0.5,0.2));
#8668=CARTESIAN_POINT('',(-0.115470053837925,-0.8,0.2));
#8669=CARTESIAN_POINT('Origin',(0.23094010767585,-0.5,0.));
#8670=CARTESIAN_POINT('',(0.115470053837925,-0.5,0.2));
#8671=CARTESIAN_POINT('',(0.115470053837925,-0.8,0.2));
#8672=CARTESIAN_POINT('Origin',(0.,-0.5,0.));
#8673=CARTESIAN_POINT('Origin',(0.,-0.8,0.));
#8674=CARTESIAN_POINT('Origin',(0.,-1.4,0.));
#8675=CARTESIAN_POINT('',(-0.24505,-1.4,3.00099698131059E-17));
#8676=CARTESIAN_POINT('Origin',(0.,-1.4,0.));
#8677=CARTESIAN_POINT('Origin',(0.375,0.5,0.));
#8678=CARTESIAN_POINT('',(-0.375,0.5,-4.59242549680257E-17));
#8679=CARTESIAN_POINT('Origin',(0.,0.5,0.));
#8680=CARTESIAN_POINT('Origin',(0.,0.475,0.));
#8681=CARTESIAN_POINT('',(-0.425,0.45,-5.20474889637625E-17));
#8682=CARTESIAN_POINT('Origin',(0.,0.45,0.));
#8683=CARTESIAN_POINT('',(-0.4,0.475,-4.89858719658941E-17));
#8684=CARTESIAN_POINT('Origin',(0.,0.24,0.));
#8685=CARTESIAN_POINT('',(-0.425,0.0299999999999998,-5.20474889637625E-17));
#8686=CARTESIAN_POINT('Origin',(0.,0.0299999999999998,0.));
#8687=CARTESIAN_POINT('',(-0.425,0.24,-5.20474889637625E-17));
#8688=CARTESIAN_POINT('Origin',(0.,0.0150000000000001,0.));
#8689=CARTESIAN_POINT('',(-0.395,4.85722573273506E-17,-4.83735485663204E-17));
#8690=CARTESIAN_POINT('Origin',(0.,0.,0.));
#8691=CARTESIAN_POINT('',(-0.41,0.0150000000000001,-5.02105187650415E-17));
#8692=CARTESIAN_POINT('Origin',(0.27,0.,0.));
#8693=CARTESIAN_POINT('',(-0.27,0.,-3.30654635769785E-17));
#8694=CARTESIAN_POINT('Origin',(0.,0.,0.));
#8695=CARTESIAN_POINT('Origin',(0.,-0.02,0.));
#8696=CARTESIAN_POINT('',(-0.24505,-0.0498999999999999,3.00099698131059E-17));
#8697=CARTESIAN_POINT('Origin',(0.,-0.0498999999999999,0.));
#8698=CARTESIAN_POINT('',(-0.26,-0.02,-3.18408167778312E-17));
#8699=CARTESIAN_POINT('Origin',(0.,-0.995,0.));
#8700=CARTESIAN_POINT('',(-0.24505,-0.995,-3.00099698131059E-17));
#9243=UNCERTAINTY_MEASURE_WITH_UNIT(LENGTH_MEASURE(0.001),#9286,
'DISTANCE_ACCURACY_VALUE',
'Maximum model space distance between geometric entities at asserted c
onnectivities');
#9255=UNCERTAINTY_MEASURE_WITH_UNIT(LENGTH_MEASURE(0.001),#9286,
'DISTANCE_ACCURACY_VALUE',
'Maximum model space distance between geometric entities at asserted c
onnectivities');
#9273=(
GEOMETRIC_REPRESENTATION_CONTEXT(3)
GLOBAL_UNCERTAINTY_ASSIGNED_CONTEXT((#9243))
GLOBAL_UNIT_ASSIGNED_CONTEXT((#9286,#9288,#9289))
REPRESENTATION_CONTEXT('','3D')
);
#9285=(
GEOMETRIC_REPRESENTATION_CONTEXT(3)
GLOBAL_UNCERTAINTY_ASSIGNED_CONTEXT((#9255))
GLOBAL_UNIT_ASSIGNED_CONTEXT((#9286,#9288,#9289))
REPRESENTATION_CONTEXT('','3D')
);
#9286=(
LENGTH_UNIT()
NAMED_UNIT(*)
SI_UNIT(.CENTI.,.METRE.)
);
#9288=(
NAMED_UNIT(*)
PLANE_ANGLE_UNIT()
SI_UNIT($,.RADIAN.)
);
#9289=(
NAMED_UNIT(*)
SI_UNIT($,.STERADIAN.)
SOLID_ANGLE_UNIT()
);
#9307=SHAPE_DEFINITION_REPRESENTATION(#9336,#9411);
#9336=PRODUCT_DEFINITION_SHAPE('',$,#9441);
#9411=SHAPE_REPRESENTATION('',(#5832),#9273);
#9423=PRODUCT_DEFINITION_CONTEXT('part definition',#9512,'design');
#9441=PRODUCT_DEFINITION('M5x14 Cap Screw (1)','M5x14 Cap Screw (1)',#9470,
#9423);
#9470=PRODUCT_DEFINITION_FORMATION('',$,#9531);
#9512=APPLICATION_CONTEXT(
'Core Data for Automotive Mechanical Design Process');
#9513=PRODUCT_CONTEXT('part definition',#9512,'mechanical');
#9531=PRODUCT('M5x14 Cap Screw (1)','M5x14 Cap Screw (1)',
'M5x14 Cap Screw (1)',(#9513));
#9613=COLOUR_RGB('Black',0.12,0.14,0.17);
#9614=FILL_AREA_STYLE_COLOUR('',#9613);
#9615=FILL_AREA_STYLE('',(#9614));
#9616=SURFACE_STYLE_FILL_AREA(#9615);
#9617=SURFACE_SIDE_STYLE('',(#9616));
#9618=SURFACE_STYLE_USAGE(.BOTH.,#9617);
#9619=PRESENTATION_STYLE_ASSIGNMENT((#9618));
ENDSEC;
END-ISO-10303-21;
